ISO-10303-21;
HEADER;
/* Generated by software containing ST-Developer
 * from STEP Tools, Inc. (www.steptools.com) 
 */

FILE_DESCRIPTION(
/* description */ ('Bracket-mounted idler roller'),
/* implementation_level */ '2;1');

FILE_NAME(
/* name */ 'Flat Washer - M6.step',
/* time_stamp */ '2026-10-28T03:26:42-07:00',
/* author */ (''),
/* organization */ (''),
/* preprocessor_version */ 'ST-DEVELOPER v20.2',
/* originating_system */ 'Autodesk Translation Framework v15.17.0.0',
/* authorisation */ '');

FILE_SCHEMA (('AUTOMOTIVE_DESIGN { 1 0 10303 214 3 1 1 }'));
ENDSEC;

DATA;
#10=MECHANICAL_DESIGN_GEOMETRIC_PRESENTATION_REPRESENTATION('',(#287),#6241);
#245=SHAPE_REPRESENTATION_RELATIONSHIP('SRR','None',#6349,#266);
#266=ADVANCED_BREP_SHAPE_REPRESENTATION('',(#316),#6225);
#287=STYLED_ITEM('',(#6545),#316);
#316=MANIFOLD_SOLID_BREP('Body1',#3189);
#366=FACE_BOUND('',#803,.T.);
#367=FACE_BOUND('',#805,.T.);
#461=PLANE('',#3562);
#462=PLANE('',#3563);
#579=FACE_OUTER_BOUND('',#800,.T.);
#580=FACE_OUTER_BOUND('',#801,.T.);
#581=FACE_OUTER_BOUND('',#802,.T.);
#582=FACE_OUTER_BOUND('',#804,.T.);
#800=EDGE_LOOP('',(#2424,#2425,#2426,#2427));
#801=EDGE_LOOP('',(#2428,#2429,#2430,#2431));
#802=EDGE_LOOP('',(#2432));
#803=EDGE_LOOP('',(#2433));
#804=EDGE_LOOP('',(#2434));
#805=EDGE_LOOP('',(#2435));
#1070=LINE('',#5242,#1252);
#1071=LINE('',#5248,#1253);
#1252=VECTOR('',#4203,0.32);
#1253=VECTOR('',#4210,0.6);
#1381=CIRCLE('',#3557,0.32);
#1382=CIRCLE('',#3558,0.32);
#1383=CIRCLE('',#3560,0.6);
#1384=CIRCLE('',#3561,0.6);
#1610=VERTEX_POINT('',#5239);
#1611=VERTEX_POINT('',#5241);
#1612=VERTEX_POINT('',#5245);
#1613=VERTEX_POINT('',#5247);
#1914=EDGE_CURVE('',#1610,#1610,#1381,.T.);
#1915=EDGE_CURVE('',#1610,#1611,#1070,.T.);
#1916=EDGE_CURVE('',#1611,#1611,#1382,.T.);
#1917=EDGE_CURVE('',#1612,#1612,#1383,.T.);
#1918=EDGE_CURVE('',#1612,#1613,#1071,.T.);
#1919=EDGE_CURVE('',#1613,#1613,#1384,.T.);
#2424=ORIENTED_EDGE('',*,*,#1914,.F.);
#2425=ORIENTED_EDGE('',*,*,#1915,.T.);
#2426=ORIENTED_EDGE('',*,*,#1916,.T.);
#2427=ORIENTED_EDGE('',*,*,#1915,.F.);
#2428=ORIENTED_EDGE('',*,*,#1917,.F.);
#2429=ORIENTED_EDGE('',*,*,#1918,.T.);
#2430=ORIENTED_EDGE('',*,*,#1919,.T.);
#2431=ORIENTED_EDGE('',*,*,#1918,.F.);
#2432=ORIENTED_EDGE('',*,*,#1917,.T.);
#2433=ORIENTED_EDGE('',*,*,#1914,.T.);
#2434=ORIENTED_EDGE('',*,*,#1919,.F.);
#2435=ORIENTED_EDGE('',*,*,#1916,.F.);
#2947=CYLINDRICAL_SURFACE('',#3556,0.32);
#2948=CYLINDRICAL_SURFACE('',#3559,0.6);
#3054=ADVANCED_FACE('',(#579),#2947,.F.);
#3055=ADVANCED_FACE('',(#580),#2948,.T.);
#3056=ADVANCED_FACE('',(#581,#366),#461,.T.);
#3057=ADVANCED_FACE('',(#582,#367),#462,.F.);
#3189=CLOSED_SHELL('',(#3054,#3055,#3056,#3057));
#3555=AXIS2_PLACEMENT_3D('',#5237,#4197,#4198);
#3556=AXIS2_PLACEMENT_3D('',#5238,#4199,#4200);
#3557=AXIS2_PLACEMENT_3D('',#5240,#4201,#4202);
#3558=AXIS2_PLACEMENT_3D('',#5243,#4204,#4205);
#3559=AXIS2_PLACEMENT_3D('',#5244,#4206,#4207);
#3560=AXIS2_PLACEMENT_3D('',#5246,#4208,#4209);
#3561=AXIS2_PLACEMENT_3D('',#5249,#4211,#4212);
#3562=AXIS2_PLACEMENT_3D('',#5250,#4213,#4214);
#3563=AXIS2_PLACEMENT_3D('',#5251,#4215,#4216);
#4197=DIRECTION('axis',(0.,0.,1.));
#4198=DIRECTION('refdir',(1.,0.,0.));
#4199=DIRECTION('center_axis',(0.,1.,0.));
#4200=DIRECTION('ref_axis',(1.,0.,0.));
#4201=DIRECTION('center_axis',(0.,-1.,0.));
#4202=DIRECTION('ref_axis',(1.,0.,0.));
#4203=DIRECTION('',(0.,-1.,0.));
#4204=DIRECTION('center_axis',(0.,-1.,0.));
#4205=DIRECTION('ref_axis',(1.,0.,0.));
#4206=DIRECTION('center_axis',(0.,1.,0.));
#4207=DIRECTION('ref_axis',(1.,0.,0.));
#4208=DIRECTION('center_axis',(0.,1.,0.));
#4209=DIRECTION('ref_axis',(1.,0.,0.));
#4210=DIRECTION('',(0.,-1.,0.));
#4211=DIRECTION('center_axis',(0.,1.,0.));
#4212=DIRECTION('ref_axis',(1.,0.,0.));
#4213=DIRECTION('center_axis',(0.,1.,0.));
#4214=DIRECTION('ref_axis',(1.,0.,0.));
#4215=DIRECTION('center_axis',(0.,1.,0.));
#4216=DIRECTION('ref_axis',(1.,0.,0.));
#5237=CARTESIAN_POINT('',(0.,0.,0.));
#5238=CARTESIAN_POINT('Origin',(0.,0.,0.));
#5239=CARTESIAN_POINT('',(-0.32,0.16,3.91886975727153E-17));
#5240=CARTESIAN_POINT('Origin',(0.,0.16,0.));
#5241=CARTESIAN_POINT('',(-0.32,0.,3.91886975727153E-17));
#5242=CARTESIAN_POINT('',(-0.32,0.,3.91886975727153E-17));
#5243=CARTESIAN_POINT('Origin',(0.,0.,0.));
#5244=CARTESIAN_POINT('Origin',(0.,0.,0.));
#5245=CARTESIAN_POINT('',(-0.6,0.16,7.34788079488412E-17));
#5246=CARTESIAN_POINT('Origin',(0.,0.16,0.));
#5247=CARTESIAN_POINT('',(-0.6,0.,7.34788079488412E-17));
#5248=CARTESIAN_POINT('',(-0.6,0.,7.34788079488412E-17));
#5249=CARTESIAN_POINT('Origin',(0.,0.,0.));
#5250=CARTESIAN_POINT('Origin',(0.,0.16,0.));
#5251=CARTESIAN_POINT('Origin',(0.,0.,0.));
#6199=UNCERTAINTY_MEASURE_WITH_UNIT(LENGTH_MEASURE(0.001),#6242,
'DISTANCE_ACCURACY_VALUE',
'Maximum model space distance between geometric entities at asserted c
onnectivities');
#6215=UNCERTAINTY_MEASURE_WITH_UNIT(LENGTH_MEASURE(0.001),#6242,
'DISTANCE_ACCURACY_VALUE',
'Maximum model space distance between geometric entities at asserted c
onnectivities');
#6225=(
GEOMETRIC_REPRESENTATION_CONTEXT(3)
GLOBAL_UNCERTAINTY_ASSIGNED_CONTEXT((#6199))
GLOBAL_UNIT_ASSIGNED_CONTEXT((#6242,#6244,#6245))
REPRESENTATION_CONTEXT('','3D')
);
#6241=(
GEOMETRIC_REPRESENTATION_CONTEXT(3)
GLOBAL_UNCERTAINTY_ASSIGNED_CONTEXT((#6215))
GLOBAL_UNIT_ASSIGNED_CONTEXT((#6242,#6244,#6245))
REPRESENTATION_CONTEXT('','3D')
);
#6242=(
LENGTH_UNIT()
NAMED_UNIT(*)
SI_UNIT(.CENTI.,.METRE.)
);
#6244=(
NAMED_UNIT(*)
PLANE_ANGLE_UNIT()
SI_UNIT($,.RADIAN.)
);
#6245=(
NAMED_UNIT(*)
SI_UNIT($,.STERADIAN.)
SOLID_ANGLE_UNIT()
);
#6255=SHAPE_DEFINITION_REPRESENTATION(#6280,#6349);
#6280=PRODUCT_DEFINITION_SHAPE('',$,#6375);
#6349=SHAPE_REPRESENTATION('',(#3555),#6225);
#6365=PRODUCT_DEFINITION_CONTEXT('part definition',#6442,'design');
#6375=PRODUCT_DEFINITION('Flat Washer - M6','Flat Washer - M6',#6400,#6365);
#6400=PRODUCT_DEFINITION_FORMATION('',$,#6453);
#6442=APPLICATION_CONTEXT(
'Core Data for Automotive Mechanical Design Process');
#6443=PRODUCT_CONTEXT('part definition',#6442,'mechanical');
#6453=PRODUCT('Flat Washer - M6','Flat Washer - M6','Flat Washer - M6',
(#6443));
#6539=COLOUR_RGB('Black',0.12,0.14,0.17);
#6540=FILL_AREA_STYLE_COLOUR('',#6539);
#6541=FILL_AREA_STYLE('',(#6540));
#6542=SURFACE_STYLE_FILL_AREA(#6541);
#6543=SURFACE_SIDE_STYLE('',(#6542));
#6544=SURFACE_STYLE_USAGE(.BOTH.,#6543);
#6545=PRESENTATION_STYLE_ASSIGNMENT((#6544));
ENDSEC;
END-ISO-10303-21;
